ISO-10303-21;
HEADER;
FILE_DESCRIPTION (('STEP AP203'),
    '1' );
FILE_NAME ('Aloris-BXA-Top-Bushing.step',
    '2026-10-07T20:09:13',
    ( '' ),
    ( '' ),
    'SwSTEP 2.0',
    'SolidWorks 2024',
    '' );
FILE_SCHEMA (( 'AUTOMOTIVE_DESIGN' ));
ENDSEC;

DATA;
#29=DIRECTION ( 'NONE',  ( -0.000000000000000000, -1.000000000000000000, -0.000000000000000000 ) ) ;
#68=EDGE_CURVE ( 'NONE', #2537, #6211, #23657, .T. ) ;
#72=DIRECTION ( 'NONE',  ( 0.000000000000000000, 0.000000000000000000, 1.000000000000000000 ) ) ;
#109=CARTESIAN_POINT ( 'NONE',  ( 0.3129697935626465366, 0.5133535954949590696, -1.110419158421684260 ) ) ;
#112=EDGE_LOOP ( 'NONE', ( #9913, #3246, #2144, #17616 ) ) ;
#157=DIRECTION ( 'NONE',  ( 0.000000000000000000, 0.000000000000000000, 1.000000000000000000 ) ) ;
#166=ORIENTED_EDGE ( 'NONE', *, *, #16153, .T. ) ;
#222=EDGE_LOOP ( 'NONE', ( #15258, #20652 ) ) ;
#230=DIRECTION ( 'NONE',  ( -0.000000000000000000, 0.2588190451025213501, -0.9659258262890680902 ) ) ;
#236=CARTESIAN_POINT ( 'NONE',  ( 0.01030609754475048101, 0.1800000000000000211, -1.243000000000000105 ) ) ;
#248=ORIENTED_EDGE ( 'NONE', *, *, #15243, .F. ) ;
#278=DIRECTION ( 'NONE',  ( 0.000000000000000000, 1.000000000000000000, 0.000000000000000000 ) ) ;
#302=DIRECTION ( 'NONE',  ( 1.000000000000000000, -0.000000000000000000, 1.224646799147353207E-16 ) ) ;
#352=CARTESIAN_POINT ( 'NONE',  ( 0.2869031291000053718, 0.6010169215856763225, -1.093172027866466278 ) ) ;
#364=ADVANCED_FACE ( 'NONE', ( #12213 ), #623, .T. ) ;
#376=CARTESIAN_POINT ( 'NONE',  ( -1.493307031895086562E-17, 0.4635611116728546865, -1.084197934689580034 ) ) ;
#385=EDGE_CURVE ( 'NONE', #4141, #5067, #8524, .T. ) ;
#394=AXIS2_PLACEMENT_3D ( 'NONE', #2859, #230, #22418 ) ;
#412=VERTEX_POINT ( 'NONE', #6339 ) ;
#428=VERTEX_POINT ( 'NONE', #21220 ) ;
#429=VECTOR ( 'NONE', #13673, 39.37007874015748143 ) ;
#470=LINE ( 'NONE', #15474, #5473 ) ;
#482=DIRECTION ( 'NONE',  ( 0.000000000000000000, 1.000000000000000000, 0.000000000000000000 ) ) ;
#528=DIRECTION ( 'NONE',  ( -0.000000000000000000, 1.000000000000000000, -0.000000000000000000 ) ) ;
#576=ORIENTED_EDGE ( 'NONE', *, *, #13809, .F. ) ;
#592=CARTESIAN_POINT ( 'NONE',  ( 0.02089524249861754446, 0.7885332705621130867, -1.079944001585411817 ) ) ;
#605=DIRECTION ( 'NONE',  ( 0.000000000000000000, 1.000000000000000000, 0.000000000000000000 ) ) ;
#623=CONICAL_SURFACE ( 'NONE', #17373, 1.243000000000000105, 0.7853981633974551624 ) ;
#658=CARTESIAN_POINT ( 'NONE',  ( 0.000000000000000000, 0.9300000000000000488, 0.000000000000000000 ) ) ;
#668=ADVANCED_FACE ( 'NONE', ( #22659 ), #20708, .F. ) ;
#761=LENGTH_MEASURE_WITH_UNIT ( LENGTH_MEASURE( 0.02539999999999999897 ), #1124 );
#775=VECTOR ( 'NONE', #528, 39.37007874015748143 ) ;
#795=VERTEX_POINT ( 'NONE', #19475 ) ;
#811=CARTESIAN_POINT ( 'NONE',  ( -0.2501893453879348028, 0.6631137783794425200, -1.085133476862891522 ) ) ;
#813=CARTESIAN_POINT ( 'NONE',  ( -1.493307031895086562E-17, 0.4842666352810564567, -1.161472000792705517 ) ) ;
#926=CARTESIAN_POINT ( 'NONE',  ( -1.515315767888941311E-17, 0.1799999999999999933, -1.242999999999999661 ) ) ;
#932=AXIS2_PLACEMENT_3D ( 'NONE', #14008, #4725, #12197 ) ;
#957=DIRECTION ( 'NONE',  ( 0.000000000000000000, 0.000000000000000000, 1.000000000000000000 ) ) ;
#961=ORIENTED_EDGE ( 'NONE', *, *, #14696, .F. ) ;
#975=EDGE_CURVE ( 'NONE', #9761, #10294, #8246, .T. ) ;
#1035=ORIENTED_EDGE ( 'NONE', *, *, #9456, .F. ) ;
#1043=CARTESIAN_POINT ( 'NONE',  ( 0.1915162893076086115, 0.2755058174450264463, -0.7251428721360214658 ) ) ;
#1059=AXIS2_PLACEMENT_3D ( 'NONE', #13640, #21058, #11801 ) ;
#1084=CARTESIAN_POINT ( 'NONE',  ( 0.000000000000000000, 0.9099999999999988098, 0.000000000000000000 ) ) ;
#1113=AXIS2_PLACEMENT_3D ( 'NONE', #6016, #4554, #12016 ) ;
#1120=DIRECTION ( 'NONE',  ( 0.000000000000000000, 0.000000000000000000, -1.000000000000000000 ) ) ;
#1124=( LENGTH_UNIT ( ) NAMED_UNIT ( * ) SI_UNIT ( $, .METRE. ) );
#1148=AXIS2_PLACEMENT_3D ( 'NONE', #15804, #6531, #17632 ) ;
#1158=CARTESIAN_POINT ( 'NONE',  ( -1.399103805173478513E-17, 0.4635611116728546865, -1.084197934689580034 ) ) ;
#1173=CARTESIAN_POINT ( 'NONE',  ( -0.1666623126836255520, 0.2230596288034553121, -1.220164406339562913 ) ) ;
#1287=CARTESIAN_POINT ( 'NONE',  ( 0.1943915731514660183, 0.2820215667548245930, -0.7243746963180275333 ) ) ;
#1293=CIRCLE ( 'NONE', #5566, 0.7500000000000001110 ) ;
#1328=ORIENTED_EDGE ( 'NONE', *, *, #16781, .T. ) ;
#1344=CARTESIAN_POINT ( 'NONE',  ( -0.02810654887314226191, 0.1573129472011667584, -0.7495061196176546758 ) ) ;
#1408=DIRECTION ( 'NONE',  ( 0.000000000000000000, 1.000000000000000000, 0.000000000000000000 ) ) ;
#1412=CLOSED_SHELL ( 'NONE', ( #12987, #6790, #364, #17901, #12182, #12813, #20594, #21833, #7393, #5463, #20530, #15707, #668, #3513, #7337, #21407, #21667, #14357, #3608 ) ) ;
#1466=CARTESIAN_POINT ( 'NONE',  ( -0.2030836461269783511, 0.4272172410711764790, -0.7219876546682471030 ) ) ;
#1531=CARTESIAN_POINT ( 'NONE',  ( 0.1672123529697439048, 0.5028202685342909595, -0.7311626644493618432 ) ) ;
#1578=EDGE_CURVE ( 'NONE', #19113, #5067, #18574, .T. ) ;
#1580=LINE ( 'NONE', #14996, #9950 ) ;
#1587=CARTESIAN_POINT ( 'NONE',  ( -0.01427084424854434090, 0.5924045552181391727, -0.7500000000000002220 ) ) ;
#1629=DIRECTION ( 'NONE',  ( -0.000000000000000000, -1.000000000000000000, -0.000000000000000000 ) ) ;
#1696=DIRECTION ( 'NONE',  ( -0.000000000000000000, 1.000000000000000000, -0.000000000000000000 ) ) ;
#1757=FACE_OUTER_BOUND ( 'NONE', #2089, .T. ) ;
#1761=DIRECTION ( 'NONE',  ( 0.000000000000000000, 0.000000000000000000, 1.000000000000000000 ) ) ;
#1786=VECTOR ( 'NONE', #10880, 39.37007874015747433 ) ;
#1804=VECTOR ( 'NONE', #6422, 39.37007874015748854 ) ;
#1861=SHAPE_REPRESENTATION ( 'Aloris-BXA-Top-Bushing', ( #9127 ), #2886 ) ;
#1865=CARTESIAN_POINT ( 'NONE',  ( 0.000000000000000000, 0.9040586665785882436, 0.000000000000000000 ) ) ;
#1940=CARTESIAN_POINT ( 'NONE',  ( 0.1579949080133604133, 0.7453945092721133703, -1.080137517429541782 ) ) ;
#2003=CARTESIAN_POINT ( 'NONE',  ( 0.000000000000000000, 0.000000000000000000, 1.223000000000000309 ) ) ;
#2027=ORIENTED_EDGE ( 'NONE', *, *, #16781, .F. ) ;
#2045=DIRECTION ( 'NONE',  ( 0.000000000000000000, 0.9659258262890680902, 0.2588190451025215166 ) ) ;
#2063=CARTESIAN_POINT ( 'NONE',  ( 0.2371649040148513243, 0.6790977978122471059, -1.083707372304768324 ) ) ;
#2085=CONICAL_SURFACE ( 'NONE', #2849, 0.7500000000000001110, 0.7853981633974482790 ) ;
#2089=EDGE_LOOP ( 'NONE', ( #8680, #3703, #7199, #248 ) ) ;
#2115=ORIENTED_EDGE ( 'NONE', *, *, #20324, .F. ) ;
#2125=VECTOR ( 'NONE', #12994, 39.37007874015747433 ) ;
#2144=ORIENTED_EDGE ( 'NONE', *, *, #12577, .T. ) ;
#2195=CARTESIAN_POINT ( 'NONE',  ( 0.2982755344125032071, 0.5726520937526655697, -1.097998983683558638 ) ) ;
#2303=DIRECTION ( 'NONE',  ( 0.000000000000000000, 0.000000000000000000, 1.000000000000000000 ) ) ;
#2311=CARTESIAN_POINT ( 'NONE',  ( 0.08213261185791022323, 0.1892061861790486077, -1.237979020847294276 ) ) ;
#2336=CIRCLE ( 'NONE', #21403, 1.223000000000000309 ) ;
#2430=CARTESIAN_POINT ( 'NONE',  ( 0.07172766006922927373, 0.7801234116097515159, -1.079864709389726452 ) ) ;
#2471=EDGE_CURVE ( 'NONE', #11248, #18852, #19867, .T. ) ;
#2482=FACE_OUTER_BOUND ( 'NONE', #21133, .T. ) ;
#2537=VERTEX_POINT ( 'NONE', #23125 ) ;
#2646=CARTESIAN_POINT ( 'NONE',  ( -0.3150149228729092199, 0.4537208395564915620, -1.126438923088229904 ) ) ;
#2754=DIRECTION ( 'NONE',  ( 0.000000000000000000, 1.000000000000000000, 0.000000000000000000 ) ) ;
#2771=AXIS2_PLACEMENT_3D ( 'NONE', #18468, #22241, #5662 ) ;
#2836=EDGE_CURVE ( 'NONE', #10294, #22559, #3402, .T. ) ;
#2849=AXIS2_PLACEMENT_3D ( 'NONE', #1084, #605, #957 ) ;
#2859=CARTESIAN_POINT ( 'NONE',  ( -1.493307031895086562E-17, 0.4842666352810564567, -1.161472000792705517 ) ) ;
#2862=CARTESIAN_POINT ( 'NONE',  ( 0.02812428215829835404, 0.1573150382780598433, -0.7495055110531126941 ) ) ;
#2872=CARTESIAN_POINT ( 'NONE',  ( -0.2825450144231913541, 0.3409525236117377789, -1.166144907693487776 ) ) ;
#2886=( GEOMETRIC_REPRESENTATION_CONTEXT ( 3 ) GLOBAL_UNCERTAINTY_ASSIGNED_CONTEXT ( ( #22892 ) ) GLOBAL_UNIT_ASSIGNED_CONTEXT ( ( #6246, #15523, #8191 ) ) REPRESENTATION_CONTEXT ( 'NONE', 'WORKASPACE' ) );
#2907=DIRECTION ( 'NONE',  ( 0.000000000000000000, 0.000000000000000000, 1.000000000000000000 ) ) ;
#2947=ORIENTED_EDGE ( 'NONE', *, *, #1578, .F. ) ;
#2989=PRODUCT_DEFINITION ( 'UNKNOWN', '', #4115, #11942 ) ;
#3005=CARTESIAN_POINT ( 'NONE',  ( -0.2081395996546885896, 0.2505969284152432808, -1.206356489598498394 ) ) ;
#3044=CARTESIAN_POINT ( 'NONE',  ( 1.522235971340160240E-16, 0.1799999999999999933, 1.243000000000000105 ) ) ;
#3115=CARTESIAN_POINT ( 'NONE',  ( 0.2031523753197612414, 0.4269420615838216970, -0.7219681823230330586 ) ) ;
#3122=CARTESIAN_POINT ( 'NONE',  ( -0.08173883172107287987, 0.7775208687833771171, -1.079850767775349940 ) ) ;
#3156=AXIS2_PLACEMENT_3D ( 'NONE', #1865, #1629, #9305 ) ;
#3169=CARTESIAN_POINT ( 'NONE',  ( -0.1918087731350874570, 0.2752783659658505355, -0.7250770848209401320 ) ) ;
#3223=DIRECTION ( 'NONE',  ( -0.000000000000000000, -1.000000000000000000, -0.000000000000000000 ) ) ;
#3224=FACE_OUTER_BOUND ( 'NONE', #23814, .T. ) ;
#3229=CARTESIAN_POINT ( 'NONE',  ( 0.1080314883215018618, 0.1837960933690710730, -0.7422718097737546206 ) ) ;
#3230=ORIENTED_EDGE ( 'NONE', *, *, #2836, .F. ) ;
#3244=ORIENTED_EDGE ( 'NONE', *, *, #22173, .F. ) ;
#3246=ORIENTED_EDGE ( 'NONE', *, *, #68, .T. ) ;
#3278=CONICAL_SURFACE ( 'NONE', #8329, 1.243000000000000105, 0.2617993877991500740 ) ;
#3286=CARTESIAN_POINT ( 'NONE',  ( -0.1989242110943551245, 0.4407889530968281400, -0.7231588590637065828 ) ) ;
#3309=ORIENTED_EDGE ( 'NONE', *, *, #68, .F. ) ;
#3402=CIRCLE ( 'NONE', #10425, 0.7700000000000013500 ) ;
#3411=CARTESIAN_POINT ( 'NONE',  ( -0.1236081594474160439, 0.5483826904852967532, -0.7397659828179361519 ) ) ;
#3436=AXIS2_PLACEMENT_3D ( 'NONE', #4806, #19813, #10318 ) ;
#3510=AXIS2_PLACEMENT_3D ( 'NONE', #14109, #12180, #17409 ) ;
#3513=ADVANCED_FACE ( 'NONE', ( #22881 ), #11583, .T. ) ;
#3518=EDGE_LOOP ( 'NONE', ( #11149, #9075, #21033, #2947 ) ) ;
#3523=CIRCLE ( 'NONE', #20648, 1.015181661097394050 ) ;
#3532=CARTESIAN_POINT ( 'NONE',  ( -0.1613775760850800489, 0.2284702193767794987, -0.7324461116423818252 ) ) ;
#3558=CARTESIAN_POINT ( 'NONE',  ( 0.000000000000000000, 0.01999999999999951469, 0.000000000000000000 ) ) ;
#3588=DIRECTION ( 'NONE',  ( 0.000000000000000000, 0.000000000000000000, 1.000000000000000000 ) ) ;
#3608=ADVANCED_FACE ( 'NONE', ( #8121 ), #6779, .F. ) ;
#3645=CARTESIAN_POINT ( 'NONE',  ( 1.090085390906250263E-17, 0.2597990586171761707, -1.138795812253956763 ) ) ;
#3703=ORIENTED_EDGE ( 'NONE', *, *, #385, .T. ) ;
#3833=CARTESIAN_POINT ( 'NONE',  ( 2.458533612140684792E-17, 0.1592944763917982509, -1.165725933896874400 ) ) ;
#3891=CIRCLE ( 'NONE', #20639, 0.3149999999999999467 ) ;
#3934=CIRCLE ( 'NONE', #5872, 1.243000000000000105 ) ;
#3943=ORIENTED_EDGE ( 'NONE', *, *, #9327, .T. ) ;
#3956=LINE ( 'NONE', #11165, #14756 ) ;
#3971=VERTEX_POINT ( 'NONE', #7742 ) ;
#3995=ORIENTED_EDGE ( 'NONE', *, *, #7681, .T. ) ;
#4004=ORIENTED_EDGE ( 'NONE', *, *, #11728, .T. ) ;
#4012=DIRECTION ( 'NONE',  ( -0.000000000000000000, -1.000000000000000000, -0.000000000000000000 ) ) ;
#4013=CARTESIAN_POINT ( 'NONE',  ( 0.2728372834934218449, 0.3240490730395221286, -1.173104893136099891 ) ) ;
#4056=EDGE_CURVE ( 'NONE', #412, #12482, #17051, .T. ) ;
#4070=FACE_OUTER_BOUND ( 'NONE', #8440, .T. ) ;
#4113=CARTESIAN_POINT ( 'NONE',  ( -1.399103805173478513E-17, 0.7678277469539112055, -1.002669935482285890 ) ) ;
#4115=PRODUCT_DEFINITION_FORMATION_WITH_SPECIFIED_SOURCE ( 'ANY', '', #10911, .NOT_KNOWN. ) ;
#4141=VERTEX_POINT ( 'NONE', #20011 ) ;
#4155=DIRECTION ( 'NONE',  ( -1.177540334020096294E-17, 0.2588190451025213501, -0.9659258262890680902 ) ) ;
#4193=CYLINDRICAL_SURFACE ( 'NONE', #1113, 0.3150000000000000577 ) ;
#4211=EDGE_LOOP ( 'NONE', ( #166, #3943 ) ) ;
#4251=CARTESIAN_POINT ( 'NONE',  ( 0.1920699496354679736, 0.7220375312147633284, -1.080957935066063857 ) ) ;
#4321=ORIENTED_EDGE ( 'NONE', *, *, #10920, .T. ) ;
#4356=DIRECTION ( 'NONE',  ( 0.000000000000000000, 0.000000000000000000, 1.000000000000000000 ) ) ;
#4366=CARTESIAN_POINT ( 'NONE',  ( 0.2825688201499270136, 0.3409968823100701374, -1.166126927630756205 ) ) ;
#4395=EDGE_LOOP ( 'NONE', ( #21377, #1328, #4004, #7021, #8656, #12424 ) ) ;
#4554=DIRECTION ( 'NONE',  ( -1.177540334020096294E-17, 0.2588190451025213501, -0.9659258262890682012 ) ) ;
#4590=CARTESIAN_POINT ( 'NONE',  ( -0.1302323571378496414, 0.2053342067589494779, -1.229370332884858863 ) ) ;
#4725=DIRECTION ( 'NONE',  ( -0.000000000000000000, -1.000000000000000000, -0.000000000000000000 ) ) ;
#4733=FACE_OUTER_BOUND ( 'NONE', #21508, .T. ) ;
#4770=DIRECTION ( 'NONE',  ( 0.000000000000000000, 0.000000000000000000, 1.000000000000000000 ) ) ;
#4788=DIMENSIONAL_EXPONENTS ( 1.000000000000000000, 0.000000000000000000, 0.000000000000000000, 0.000000000000000000, 0.000000000000000000, 0.000000000000000000, 0.000000000000000000 ) ;
#4806=CARTESIAN_POINT ( 'NONE',  ( 0.000000000000000000, 0.000000000000000000, 0.000000000000000000 ) ) ;
#4818=CARTESIAN_POINT ( 'NONE',  ( -0.07172508667748003774, 0.7801245175820353817, -1.079864711465235327 ) ) ;
#4854=CARTESIAN_POINT ( 'NONE',  ( 0.000000000000000000, 0.000000000000000000, 0.000000000000000000 ) ) ;
#4897=ORIENTED_EDGE ( 'NONE', *, *, #5712, .F. ) ;
#4936=CARTESIAN_POINT ( 'NONE',  ( 0.1704550048180128174, 0.2392892945790311421, -0.7304142363202623667 ) ) ;
#4944=CARTESIAN_POINT ( 'NONE',  ( -0.1015928384594063510, 0.7712678869592031194, -1.079846914997397489 ) ) ;
#4997=ORIENTED_EDGE ( 'NONE', *, *, #8124, .F. ) ;
#5002=VECTOR ( 'NONE', #5783, 39.37007874015748143 ) ;
#5045=AXIS2_PLACEMENT_3D ( 'NONE', #18283, #1696, #16458 ) ;
#5048=ORIENTED_EDGE ( 'NONE', *, *, #8124, .T. ) ;
#5054=CARTESIAN_POINT ( 'NONE',  ( 0.05567750539902905499, 0.5846369443820266243, -0.7480565307454484225 ) ) ;
#5067=VERTEX_POINT ( 'NONE', #9812 ) ;
#5111=CARTESIAN_POINT ( 'NONE',  ( -0.09538643074235236829, 0.1770772191347038393, -0.7440238671003180926 ) ) ;
#5122=ORIENTED_EDGE ( 'NONE', *, *, #385, .F. ) ;
#5147=CIRCLE ( 'NONE', #9849, 0.3149999999999999467 ) ;
#5169=CYLINDRICAL_SURFACE ( 'NONE', #18909, 1.243000000000000105 ) ;
#5176=CARTESIAN_POINT ( 'NONE',  ( 0.1419858815579627120, 0.2082143347958492208, -0.7365060972889347912 ) ) ;
#5229=DIRECTION ( 'NONE',  ( 0.000000000000000000, 0.000000000000000000, 1.000000000000000000 ) ) ;
#5232=CARTESIAN_POINT ( 'NONE',  ( -0.01405487212420455066, 0.1559577530655004984, -0.7499012348325908572 ) ) ;
#5253=CARTESIAN_POINT ( 'NONE',  ( 1.090085390906250263E-17, 0.2805045822253778853, -1.216069878357082468 ) ) ;
#5262=VERTEX_POINT ( 'NONE', #18978 ) ;
#5304=CARTESIAN_POINT ( 'NONE',  ( 0.1616910252715724194, 0.2282749528075390943, -0.7324324093404095404 ) ) ;
#5417=EDGE_LOOP ( 'NONE', ( #11327, #17265 ) ) ;
#5463=ADVANCED_FACE ( 'NONE', ( #3224, #23453 ), #12396, .F. ) ;
#5473=VECTOR ( 'NONE', #4012, 39.37007874015748143 ) ;
#5526=DIRECTION ( 'NONE',  ( 0.000000000000000000, 0.000000000000000000, 1.000000000000000000 ) ) ;
#5538=ORIENTED_EDGE ( 'NONE', *, *, #4056, .F. ) ;
#5566=AXIS2_PLACEMENT_3D ( 'NONE', #11174, #10813, #20192 ) ;
#5662=DIRECTION ( 'NONE',  ( 0.000000000000000000, 0.000000000000000000, 1.000000000000000000 ) ) ;
#5711=VERTEX_POINT ( 'NONE', #2003 ) ;
#5712=EDGE_CURVE ( 'NONE', #3971, #11248, #20537, .T. ) ;
#5726=CARTESIAN_POINT ( 'NONE',  ( 0.2674045363888666316, 0.6373041478666018333, -1.088102446297350534 ) ) ;
#5783=DIRECTION ( 'NONE',  ( -0.000000000000000000, 1.000000000000000000, -0.000000000000000000 ) ) ;
#5839=CARTESIAN_POINT ( 'NONE',  ( 0.1923949478952308167, 0.2387739693004125863, -1.212204774773908866 ) ) ;
#5872=AXIS2_PLACEMENT_3D ( 'NONE', #22226, #482, #5526 ) ;
#5941=LINE ( 'NONE', #4113, #10484 ) ;
#5948=DIRECTION ( 'NONE',  ( -0.000000000000000000, 1.000000000000000000, -0.000000000000000000 ) ) ;
#5965=LINE ( 'NONE', #11025, #429 ) ;
#6016=CARTESIAN_POINT ( 'NONE',  ( -1.399103805173478513E-17, 0.4635611116728546865, -1.084197934689580034 ) ) ;
#6077=CARTESIAN_POINT ( 'NONE',  ( 0.1398094450097594477, 0.2094524755924680182, -1.227205251919106344 ) ) ;
#6190=VERTEX_POINT ( 'NONE', #7760 ) ;
#6195=CARTESIAN_POINT ( 'NONE',  ( 0.2675580960581577239, 0.3158763822996886739, -1.176569835631964045 ) ) ;
#6211=VERTEX_POINT ( 'NONE', #3645 ) ;
#6217=CARTESIAN_POINT ( 'NONE',  ( 0.000000000000000000, 0.01999999999999951469, 0.000000000000000000 ) ) ;
#6246=( CONVERSION_BASED_UNIT ( 'INCH', #761 ) LENGTH_UNIT ( ) NAMED_UNIT ( #4788 ) );
#6278=VERTEX_POINT ( 'NONE', #16339 ) ;
#6323=DIRECTION ( 'NONE',  ( 0.000000000000000000, 1.000000000000000000, 0.000000000000000000 ) ) ;
#6339=CARTESIAN_POINT ( 'NONE',  ( -1.403438536077215402E-16, 0.9040586665785882436, -1.048989065017511546 ) ) ;
#6415=CARTESIAN_POINT ( 'NONE',  ( -0.3048832246468780593, 0.3952586090242287686, -1.145453902462662432 ) ) ;
#6417=DIRECTION ( 'NONE',  ( -0.000000000000000000, 0.2588190451025213501, -0.9659258262890680902 ) ) ;
#6422=DIRECTION ( 'NONE',  ( 8.659560562354932858E-17, 0.7071067811865474617, -0.7071067811865474617 ) ) ;
#6484=ORIENTED_EDGE ( 'NONE', *, *, #9456, .T. ) ;
#6488=EDGE_CURVE ( 'NONE', #6278, #2537, #20887, .T. ) ;
#6531=DIRECTION ( 'NONE',  ( -0.000000000000000000, -1.000000000000000000, -0.000000000000000000 ) ) ;
#6534=CARTESIAN_POINT ( 'NONE',  ( -0.1836571724648604909, 0.7278005416041625208, -1.080755778418241109 ) ) ;
#6554=CARTESIAN_POINT ( 'NONE',  ( -1.515315767888941311E-17, 0.1799999999999999933, -1.242999999999999661 ) ) ;
#6620=EDGE_CURVE ( 'NONE', #6190, #22559, #3956, .T. ) ;
#6646=CARTESIAN_POINT ( 'NONE',  ( 0.1312456515338671081, 0.1993400706575450265, -0.7385206977513997240 ) ) ;
#6655=CARTESIAN_POINT ( 'NONE',  ( -0.2947723466326633290, 0.5822653189610053071, -1.096280161095893435 ) ) ;
#6661=EDGE_CURVE ( 'NONE', #6278, #9761, #7613, .T. ) ;
#6681=DIRECTION ( 'NONE',  ( -1.177540334020096602E-17, 0.2588190451025213501, -0.9659258262890682012 ) ) ;
#6761=DIRECTION ( 'NONE',  ( 0.000000000000000000, 0.9659258262890680902, 0.2588190451025214611 ) ) ;
#6777=CARTESIAN_POINT ( 'NONE',  ( -0.1018020887675157859, 0.1946365182022625206, -1.235038816363745129 ) ) ;
#6779=CYLINDRICAL_SURFACE ( 'NONE', #7298, 0.2109499999999996656 ) ;
#6790=ADVANCED_FACE ( 'NONE', ( #4070 ), #4193, .F. ) ;
#6856=ORIENTED_EDGE ( 'NONE', *, *, #9327, .F. ) ;
#6928=DIRECTION ( 'NONE',  ( 0.000000000000000000, 0.9659258262890682012, 0.2588190451025213501 ) ) ;
#6955=CARTESIAN_POINT ( 'NONE',  ( -0.1854441301479783366, 0.2626830736182380610, -0.7267533148750512373 ) ) ;
#6973=FACE_OUTER_BOUND ( 'NONE', #18495, .T. ) ;
#7007=ORIENTED_EDGE ( 'NONE', *, *, #7681, .F. ) ;
#7021=ORIENTED_EDGE ( 'NONE', *, *, #12849, .T. ) ;
#7033=AXIS2_PLACEMENT_3D ( 'NONE', #21440, #6681, #6928 ) ;
#7046=AXIS2_PLACEMENT_3D ( 'NONE', #376, #4155, #19510 ) ;
#7078=CARTESIAN_POINT ( 'NONE',  ( -0.2088978631689275278, 0.3995044321532407738, -0.7203268866154032279 ) ) ;
#7097=DIRECTION ( 'NONE',  ( -0.000000000000000000, -1.000000000000000000, -0.000000000000000000 ) ) ;
#7109=CARTESIAN_POINT ( 'NONE',  ( -1.399103805173478513E-17, 0.7678277469539112055, -1.002669935482285890 ) ) ;
#7141=CARTESIAN_POINT ( 'NONE',  ( 0.2055726870590093569, 0.3152965443106340304, -0.7212806285457649125 ) ) ;
#7197=CARTESIAN_POINT ( 'NONE',  ( -0.03517071929010351372, 0.1583405707270942042, -0.7492072654479503546 ) ) ;
#7199=ORIENTED_EDGE ( 'NONE', *, *, #14895, .T. ) ;
#7298=AXIS2_PLACEMENT_3D ( 'NONE', #813, #6417, #23346 ) ;
#7317=CARTESIAN_POINT ( 'NONE',  ( 9.184120737366631376E-17, 0.1556215347031258134, -0.7500000000000001110 ) ) ;
#7337=ADVANCED_FACE ( 'NONE', ( #10092 ), #22929, .F. ) ;
#7393=ADVANCED_FACE ( 'NONE', ( #13747 ), #12046, .T. ) ;
#7398=AXIS2_PLACEMENT_3D ( 'NONE', #19411, #17586, #1120 ) ;
#7435=DIRECTION ( 'NONE',  ( -0.000000000000000000, 1.000000000000000000, -0.000000000000000000 ) ) ;
#7446=CIRCLE ( 'NONE', #12914, 0.7500000000000001110 ) ;
#7476=DIRECTION ( 'NONE',  ( 0.000000000000000000, 0.000000000000000000, 1.000000000000000000 ) ) ;
#7484=ORIENTED_EDGE ( 'NONE', *, *, #13192, .F. ) ;
#7491=VERTEX_POINT ( 'NONE', #8733 ) ;
#7613=LINE ( 'NONE', #22487, #5002 ) ;
#7640=VECTOR ( 'NONE', #13684, 39.37007874015748143 ) ;
#7672=CARTESIAN_POINT ( 'NONE',  ( 0.1668575117781267991, 0.2231724005212394890, -1.220106870630045748 ) ) ;
#7681=EDGE_CURVE ( 'NONE', #10527, #18852, #5941, .T. ) ;
#7742=CARTESIAN_POINT ( 'NONE',  ( 2.458533612140684792E-17, 0.1592944763917982509, -1.165725933896874400 ) ) ;
#7760=CARTESIAN_POINT ( 'NONE',  ( 0.000000000000000000, 0.9099999999999988098, 0.7500000000000001110 ) ) ;
#7793=CARTESIAN_POINT ( 'NONE',  ( 0.08171969123827281523, 0.7775251020733242591, -1.079850811755443951 ) ) ;
#7845=ORIENTED_EDGE ( 'NONE', *, *, #14566, .T. ) ;
#7883=LINE ( 'NONE', #15335, #8575 ) ;
#7902=CARTESIAN_POINT ( 'NONE',  ( 0.04131066265099773288, 0.1822999795785922583, -1.241739854591859871 ) ) ;
#7949=AXIS2_PLACEMENT_3D ( 'NONE', #15877, #23293, #4770 ) ;
#7951=APPLICATION_CONTEXT ( 'configuration controlled 3d designs of mechanical parts and assemblies' ) ;
#7957=MECHANICAL_CONTEXT ( 'NONE', #8407, 'mechanical' ) ;
#7986=EDGE_LOOP ( 'NONE', ( #4897, #16926, #3995, #20064 ) ) ;
#8078=AXIS2_PLACEMENT_3D ( 'NONE', #18966, #302, #9338 ) ;
#8121=FACE_OUTER_BOUND ( 'NONE', #14655, .T. ) ;
#8124=EDGE_CURVE ( 'NONE', #5262, #5711, #2336, .T. ) ;
#8131=DIRECTION ( 'NONE',  ( -0.000000000000000000, -1.000000000000000000, -0.000000000000000000 ) ) ;
#8184=VECTOR ( 'NONE', #21677, 39.37007874015748143 ) ;
#8191=( NAMED_UNIT ( * ) SI_UNIT ( $, .STERADIAN. ) SOLID_ANGLE_UNIT ( ) );
#8216=AXIS2_PLACEMENT_3D ( 'NONE', #10732, #16821, #20354 ) ;
#8246=LINE ( 'NONE', #23113, #1804 ) ;
#8297=EDGE_CURVE ( 'NONE', #412, #428, #17131, .T. ) ;
#8329=AXIS2_PLACEMENT_3D ( 'NONE', #21957, #7097, #14659 ) ;
#8343=CARTESIAN_POINT ( 'NONE',  ( -1.493307031895086562E-17, 0.4635611116728546865, -1.084197934689580034 ) ) ;
#8407=APPLICATION_CONTEXT ( 'configuration controlled 3d designs of mechanical parts and assemblies' ) ;
#8440=EDGE_LOOP ( 'NONE', ( #6856, #11807, #961, #7007 ) ) ;
#8458=ORIENTED_EDGE ( 'NONE', *, *, #19717, .T. ) ;
#8472=CARTESIAN_POINT ( 'NONE',  ( 0.007029742477379865087, 0.1556215347031258134, -0.7499999999999998890 ) ) ;
#8479=CARTESIAN_POINT ( 'NONE',  ( -0.1920051058283686329, 0.7214575884338099154, -1.081025299797705008 ) ) ;
#8524=LINE ( 'NONE', #3044, #7640 ) ;
#8575=VECTOR ( 'NONE', #9852, 39.37007874015748143 ) ;
#8604=CARTESIAN_POINT ( 'NONE',  ( 0.06924143819089124963, 0.5799707351147035395, -0.7469066312677832276 ) ) ;
#8611=CARTESIAN_POINT ( 'NONE',  ( -0.1395219119112078299, 0.2093243512325797528, -1.227272371974961418 ) ) ;
#8615=TOROIDAL_SURFACE ( 'NONE', #12135, 1.015181661097394050, 0.03500000000000000333 ) ;
#8656=ORIENTED_EDGE ( 'NONE', *, *, #6661, .F. ) ;
#8663=AXIS2_PLACEMENT_3D ( 'NONE', #23022, #6323, #10121 ) ;
#8680=ORIENTED_EDGE ( 'NONE', *, *, #11798, .F. ) ;
#8733=CARTESIAN_POINT ( 'NONE',  ( 0.000000000000000000, 0.000000000000000000, 0.7500000000000001110 ) ) ;
#8741=AXIS2_PLACEMENT_3D ( 'NONE', #15816, #8131, #4356 ) ;
#8901=CARTESIAN_POINT ( 'NONE',  ( -0.1566782819544844385, 0.2231665291434455078, -0.7334692270860763141 ) ) ;
#8955=CIRCLE ( 'NONE', #8216, 0.7500000000000001110 ) ;
#9023=CARTESIAN_POINT ( 'NONE',  ( -0.1419325426031897985, 0.2081706596913604768, -0.7365160675939218526 ) ) ;
#9075=ORIENTED_EDGE ( 'NONE', *, *, #20953, .F. ) ;
#9127=AXIS2_PLACEMENT_3D ( 'NONE', #15878, #23181, #23294 ) ;
#9131=AXIS2_PLACEMENT_3D ( 'NONE', #1158, #16038, #6761 ) ;
#9140=CARTESIAN_POINT ( 'NONE',  ( -0.1444244075563662910, 0.5295867991985312440, -0.7359786888858205200 ) ) ;
#9170=DIRECTION ( 'NONE',  ( -0.000000000000000000, 1.000000000000000000, -0.000000000000000000 ) ) ;
#9305=DIRECTION ( 'NONE',  ( 0.000000000000000000, 0.000000000000000000, -1.000000000000000000 ) ) ;
#9327=EDGE_CURVE ( 'NONE', #3971, #10527, #3891, .T. ) ;
#9338=DIRECTION ( 'NONE',  ( 1.224646799147352468E-16, 0.000000000000000000, -1.000000000000000000 ) ) ;
#9387=CARTESIAN_POINT ( 'NONE',  ( 0.1113574050366882423, 0.7676397398856372734, -1.079857189324826550 ) ) ;
#9419=DIRECTION ( 'NONE',  ( -0.000000000000000000, 0.2588190451025213501, -0.9659258262890682012 ) ) ;
#9440=DIRECTION ( 'NONE',  ( -1.177540334020096140E-17, 0.2588190451025212946, -0.9659258262890679791 ) ) ;
#9456=EDGE_CURVE ( 'NONE', #428, #795, #14417, .T. ) ;
#9484=CARTESIAN_POINT ( 'NONE',  ( -1.399103805173478513E-17, 0.4635611116728546865, -1.084197934689580034 ) ) ;
#9543=CONICAL_SURFACE ( 'NONE', #23146, 1.243000000000000105, 0.7853981633974551624 ) ;
#9626=CARTESIAN_POINT ( 'NONE',  ( 0.3048633063337730653, 0.3951878887010597530, -1.145478839108450941 ) ) ;
#9748=CARTESIAN_POINT ( 'NONE',  ( 0.1399608807533026522, 0.7553615324114533180, -1.079965574340326917 ) ) ;
#9761=VERTEX_POINT ( 'NONE', #18727 ) ;
#9803=ORIENTED_EDGE ( 'NONE', *, *, #6661, .T. ) ;
#9812=CARTESIAN_POINT ( 'NONE',  ( 1.522235971340160240E-16, 0.01999999999999951469, 1.243000000000000105 ) ) ;
#9849=AXIS2_PLACEMENT_3D ( 'NONE', #9484, #22524, #2045 ) ;
#9852=DIRECTION ( 'NONE',  ( 8.659560562354992023E-17, 0.7071067811865426878, -0.7071067811865523467 ) ) ;
#9872=CARTESIAN_POINT ( 'NONE',  ( 0.2082367465038017507, 0.2506576595349946368, -1.206325088425369563 ) ) ;
#9913=ORIENTED_EDGE ( 'NONE', *, *, #10920, .F. ) ;
#9918=SHAPE_REPRESENTATION_RELATIONSHIP ( 'NONE' , 'NONE' ,  #1861, #19865 ) ;
#9948=ORIENTED_EDGE ( 'NONE', *, *, #22173, .T. ) ;
#9950=VECTOR ( 'NONE', #22176, 39.37007874015747433 ) ;
#9970=EDGE_CURVE ( 'NONE', #6278, #23184, #11496, .T. ) ;
#10088=CARTESIAN_POINT ( 'NONE',  ( 0.000000000000000000, 0.9300000000000000488, 0.000000000000000000 ) ) ;
#10092=FACE_OUTER_BOUND ( 'NONE', #23029, .T. ) ;
#10095=CARTESIAN_POINT ( 'NONE',  ( -0.2503918017774145466, 0.2920750874296680899, -1.186911552162836836 ) ) ;
#10121=DIRECTION ( 'NONE',  ( 0.000000000000000000, -0.000000000000000000, 1.000000000000000000 ) ) ;
#10201=FACE_OUTER_BOUND ( 'NONE', #112, .T. ) ;
#10208=DIRECTION ( 'NONE',  ( 0.000000000000000000, 0.000000000000000000, 1.000000000000000000 ) ) ;
#10235=FACE_OUTER_BOUND ( 'NONE', #4211, .T. ) ;
#10265=CARTESIAN_POINT ( 'NONE',  ( -1.493307031895086562E-17, 0.6673231647285333690, -1.029600057125203305 ) ) ;
#10294=VERTEX_POINT ( 'NONE', #13127 ) ;
#10318=DIRECTION ( 'NONE',  ( 0.000000000000000000, -0.000000000000000000, 1.000000000000000000 ) ) ;
#10324=CARTESIAN_POINT ( 'NONE',  ( 0.01406054063584270125, 0.1559579195750173675, -0.7499011851857120270 ) ) ;
#10331=CARTESIAN_POINT ( 'NONE',  ( -0.2371368682194363309, 0.2772055556030146861, -1.193725331483267205 ) ) ;
#10425=AXIS2_PLACEMENT_3D ( 'NONE', #658, #15657, #12377 ) ;
#10476=PLANE ( 'NONE',  #7033 ) ;
#10484=VECTOR ( 'NONE', #11571, 39.37007874015748854 ) ;
#10501=CARTESIAN_POINT ( 'NONE',  ( -0.06946101865132212061, 0.1664525777826655062, -0.7468903887938297403 ) ) ;
#10527=VERTEX_POINT ( 'NONE', #7109 ) ;
#10569=DIRECTION ( 'NONE',  ( 0.000000000000000000, 0.000000000000000000, 1.000000000000000000 ) ) ;
#10573=CARTESIAN_POINT ( 'NONE',  ( -0.2732709761971058859, 0.6284990011602862303, -1.089116489376853014 ) ) ;
#10619=CARTESIAN_POINT ( 'NONE',  ( -0.1741657073137734824, 0.2450887835488839428, -0.7295075619333545314 ) ) ;
#10732=CARTESIAN_POINT ( 'NONE',  ( 0.000000000000000000, 0.9099999999999988098, 0.000000000000000000 ) ) ;
#10806=CARTESIAN_POINT ( 'NONE',  ( 0.1067006177585113069, 0.5609178672485701789, -0.7424598444660861496 ) ) ;
#10813=DIRECTION ( 'NONE',  ( -0.000000000000000000, -1.000000000000000000, -0.000000000000000000 ) ) ;
#10832=CARTESIAN_POINT ( 'NONE',  ( 0.000000000000000000, 0.01999999999999951469, 1.243000000000000105 ) ) ;
#10861=CARTESIAN_POINT ( 'NONE',  ( -0.09471748901421209177, 0.5680892572981176558, -0.7441037951239753978 ) ) ;
#10880=DIRECTION ( 'NONE',  ( -0.000000000000000000, 0.2588190451025213501, -0.9659258262890682012 ) ) ;
#10911=PRODUCT ( 'Aloris-BXA-Top-Bushing', 'Aloris-BXA-Top-Bushing', '', ( #7957 ) ) ;
#10920=EDGE_CURVE ( 'NONE', #2537, #6278, #12940, .T. ) ;
#10921=FACE_OUTER_BOUND ( 'NONE', #12397, .T. ) ;
#10924=EDGE_LOOP ( 'NONE', ( #8458, #18757 ) ) ;
#10983=CARTESIAN_POINT ( 'NONE',  ( -0.07574842331155759445, 0.5769426278466130986, -0.7461920942536031109 ) ) ;
#10986=ORIENTED_EDGE ( 'NONE', *, *, #6488, .F. ) ;
#11025=CARTESIAN_POINT ( 'NONE',  ( 0.000000000000000000, -3.937007874019685528E-05, 0.7500000000000001110 ) ) ;
#11130=AXIS2_PLACEMENT_3D ( 'NONE', #14708, #1408, #3588 ) ;
#11149=ORIENTED_EDGE ( 'NONE', *, *, #14566, .F. ) ;
#11165=CARTESIAN_POINT ( 'NONE',  ( 0.000000000000000000, 0.9099999999999988098, 0.7500000000000001110 ) ) ;
#11174=CARTESIAN_POINT ( 'NONE',  ( 0.000000000000000000, 0.000000000000000000, 0.000000000000000000 ) ) ;
#11248=VERTEX_POINT ( 'NONE', #6554 ) ;
#11249=ORIENTED_EDGE ( 'NONE', *, *, #11314, .F. ) ;
#11314=EDGE_CURVE ( 'NONE', #5711, #5067, #12671, .T. ) ;
#11327=ORIENTED_EDGE ( 'NONE', *, *, #17962, .F. ) ;
#11339=CARTESIAN_POINT ( 'NONE',  ( 0.1580470504400612042, 0.2183455552519602272, -1.222587402392238065 ) ) ;
#11452=CARTESIAN_POINT ( 'NONE',  ( 0.000000000000000000, -3.937007874019685528E-05, 0.000000000000000000 ) ) ;
#11461=CARTESIAN_POINT ( 'NONE',  ( 0.2947906553666733709, 0.5822185911807998826, -1.096288212844231724 ) ) ;
#11496=LINE ( 'NONE', #11615, #18690 ) ;
#11543=ORIENTED_EDGE ( 'NONE', *, *, #9970, .T. ) ;
#11571=DIRECTION ( 'NONE',  ( -1.177540334020096140E-17, 0.2588190451025212946, -0.9659258262890679791 ) ) ;
#11583=TOROIDAL_SURFACE ( 'NONE', #1059, 1.015181661097394050, 0.03500000000000000333 ) ;
#11586=CARTESIAN_POINT ( 'NONE',  ( -1.515315767888941311E-17, 0.1799999999999999933, -1.242999999999999661 ) ) ;
#11615=CARTESIAN_POINT ( 'NONE',  ( -1.493307031895086562E-17, 0.6880286883367350281, -1.106874123228328788 ) ) ;
#11618=ORIENTED_EDGE ( 'NONE', *, *, #975, .T. ) ;
#11627=ORIENTED_EDGE ( 'NONE', *, *, #20163, .T. ) ;
#11634=VECTOR ( 'NONE', #9440, 39.37007874015748854 ) ;
#11703=CARTESIAN_POINT ( 'NONE',  ( 0.2988972802092635939, 0.3766541926404427532, -1.152205679622806622 ) ) ;
#11728=EDGE_CURVE ( 'NONE', #7491, #6190, #5965, .T. ) ;
#11755=EDGE_CURVE ( 'NONE', #428, #412, #19120, .T. ) ;
#11798=EDGE_CURVE ( 'NONE', #4141, #11248, #3934, .T. ) ;
#11801=DIRECTION ( 'NONE',  ( 0.000000000000000000, 0.000000000000000000, 1.000000000000000000 ) ) ;
#11807=ORIENTED_EDGE ( 'NONE', *, *, #5712, .T. ) ;
#11820=ORIENTED_EDGE ( 'NONE', *, *, #20953, .T. ) ;
#11935=EDGE_CURVE ( 'NONE', #7491, #16373, #7446, .T. ) ;
#11942=DESIGN_CONTEXT ( 'detailed design', #7951, 'design' ) ;
#12016=DIRECTION ( 'NONE',  ( 0.000000000000000000, 0.9659258262890680902, 0.2588190451025214611 ) ) ;
#12046=CYLINDRICAL_SURFACE ( 'NONE', #1148, 1.243000000000000105 ) ;
#12049=CARTESIAN_POINT ( 'NONE',  ( -0.1923458283087008946, 0.2387311634213351574, -1.212225631218351030 ) ) ;
#12094=CIRCLE ( 'NONE', #2771, 0.7500000000000001110 ) ;
#12128=ORIENTED_EDGE ( 'NONE', *, *, #2471, .T. ) ;
#12135=AXIS2_PLACEMENT_3D ( 'NONE', #14939, #14579, #1761 ) ;
#12171=CARTESIAN_POINT ( 'NONE',  ( -0.3068635116330460932, 0.5432355565805958575, -1.103811322571780940 ) ) ;
#12180=DIRECTION ( 'NONE',  ( -1.000000000000000000, 0.000000000000000000, 0.000000000000000000 ) ) ;
#12182=ADVANCED_FACE ( 'NONE', ( #10921 ), #8615, .T. ) ;
#12197=DIRECTION ( 'NONE',  ( 0.000000000000000000, 0.000000000000000000, 1.000000000000000000 ) ) ;
#12213=FACE_OUTER_BOUND ( 'NONE', #14942, .T. ) ;
#12226=CIRCLE ( 'NONE', #15703, 0.2109499999999996100 ) ;
#12272=FACE_OUTER_BOUND ( 'NONE', #7986, .T. ) ;
#12288=CARTESIAN_POINT ( 'NONE',  ( -0.3129558008298474192, 0.5134348993187674015, -1.110400460330370542 ) ) ;
#12297=ORIENTED_EDGE ( 'NONE', *, *, #14696, .T. ) ;
#12329=DIRECTION ( 'NONE',  ( 0.000000000000000000, 0.000000000000000000, 1.000000000000000000 ) ) ;
#12343=CARTESIAN_POINT ( 'NONE',  ( -0.2112264183043934263, 0.3573296004273216475, -0.7196412499502125026 ) ) ;
#12377=DIRECTION ( 'NONE',  ( 0.000000000000000000, 0.000000000000000000, 1.000000000000000000 ) ) ;
#12395=CARTESIAN_POINT ( 'NONE',  ( 0.000000000000000000, 0.1799999999999999933, 0.000000000000000000 ) ) ;
#12396=PLANE ( 'NONE',  #3436 ) ;
#12397=EDGE_LOOP ( 'NONE', ( #13784, #17263, #576, #1035 ) ) ;
#12408=CARTESIAN_POINT ( 'NONE',  ( -0.2371691208608801282, 0.6790887934624100231, -1.083708510387177082 ) ) ;
#12424=ORIENTED_EDGE ( 'NONE', *, *, #6488, .T. ) ;
#12482=VERTEX_POINT ( 'NONE', #12968 ) ;
#12523=CARTESIAN_POINT ( 'NONE',  ( 0.1821285033488274085, 0.4790585882761230763, -0.7275905587198648883 ) ) ;
#12577=EDGE_CURVE ( 'NONE', #6211, #23184, #17560, .T. ) ;
#12578=CARTESIAN_POINT ( 'NONE',  ( -0.007027963641057663469, 0.1556215347031258966, -0.7500000000000003331 ) ) ;
#12645=CARTESIAN_POINT ( 'NONE',  ( 0.09542861826504350775, 0.1770968263373798313, -0.7440186716057061167 ) ) ;
#12671=LINE ( 'NONE', #10832, #8184 ) ;
#12674=ORIENTED_EDGE ( 'NONE', *, *, #20163, .F. ) ;
#12705=CARTESIAN_POINT ( 'NONE',  ( -0.1394808293864866489, 0.5344994213878939693, -0.7369348578741334865 ) ) ;
#12767=CARTESIAN_POINT ( 'NONE',  ( 0.03519696264514372147, 0.1583449576561939409, -0.7492059971800684171 ) ) ;
#12813=ADVANCED_FACE ( 'NONE', ( #22056 ), #22177, .F. ) ;
#12849=EDGE_CURVE ( 'NONE', #6190, #9761, #8955, .T. ) ;
#12914=AXIS2_PLACEMENT_3D ( 'NONE', #4854, #21330, #2907 ) ;
#12940=B_SPLINE_CURVE_WITH_KNOTS ( 'NONE', 3,
 ( #7317, #12578, #5232, #1344, #7197, #18170, #10501, #5111, #22183, #23639, #9023, #8901, #3532, #19999, #10619, #6955, #3169, #23516, #14642, #20120, #12343, #16102, #7078, #1466, #3286, #18290, #14273, #14517, #14767, #9140, #12705, #16227, #3411, #14397, #10861, #10983, #18409, #16585, #17933, #19759, #1587, #16464 ),
 .UNSPECIFIED., .F., .F.,
 ( 4, 2, 2, 2, 2, 2, 2, 2, 2, 2, 2, 2, 2, 2, 2, 2, 2, 2, 2, 2, 4 ),
 ( 0.01713591359826903762, 0.01767127539367114447, 0.01820663718907325479, 0.01927736077987746849, 0.02034808437068168566, 0.02141880796148589935, 0.02195416975688800620, 0.02248953155229011652, 0.02356025514309433022, 0.02463097873389854045, 0.02570170232470275415, 0.02677242591550696785, 0.02784314950631118502, 0.02891387309711539871, 0.02998459668791961241, 0.03051995848332171926, 0.03105532027872382611, 0.03212604386952803981, 0.03266140566493014319, 0.03319676746033224657, 0.03426749105113646027 ),
 .UNSPECIFIED. ) ;
#12968=CARTESIAN_POINT ( 'NONE',  ( 1.263940036315143372E-16, 0.9300000000000000488, -1.015181661097394050 ) ) ;
#12987=ADVANCED_FACE ( 'NONE', ( #10201 ), #23095, .F. ) ;
#12994=DIRECTION ( 'NONE',  ( 0.000000000000000000, -0.9659258262890682012, 0.2588190451025213501 ) ) ;
#13127=CARTESIAN_POINT ( 'NONE',  ( 9.429780353434637026E-17, 0.9300000000000000488, -0.7700000000000013500 ) ) ;
#13185=CARTESIAN_POINT ( 'NONE',  ( 0.2825004670929462391, 0.6102487556800120228, -1.091766657629984483 ) ) ;
#13192=EDGE_CURVE ( 'NONE', #9761, #6190, #12094, .T. ) ;
#13302=CARTESIAN_POINT ( 'NONE',  ( 0.3068681509333300861, 0.5432192738334535864, -1.103814563215323785 ) ) ;
#13407=EDGE_CURVE ( 'NONE', #16373, #2537, #21261, .T. ) ;
#13543=CARTESIAN_POINT ( 'NONE',  ( 0.1303878333502071496, 0.2053964056049825126, -1.229337499098527076 ) ) ;
#13640=CARTESIAN_POINT ( 'NONE',  ( 0.000000000000000000, 0.8949999999999999067, 0.000000000000000000 ) ) ;
#13673=DIRECTION ( 'NONE',  ( -0.000000000000000000, 1.000000000000000000, -0.000000000000000000 ) ) ;
#13684=DIRECTION ( 'NONE',  ( -0.000000000000000000, -1.000000000000000000, -0.000000000000000000 ) ) ;
#13715=EDGE_LOOP ( 'NONE', ( #20344, #2027 ) ) ;
#13747=FACE_OUTER_BOUND ( 'NONE', #22840, .T. ) ;
#13784=ORIENTED_EDGE ( 'NONE', *, *, #8297, .F. ) ;
#13809=EDGE_CURVE ( 'NONE', #795, #12482, #3523, .T. ) ;
#13869=CARTESIAN_POINT ( 'NONE',  ( -0.2869978706053274431, 0.3497335006013223002, -1.162630022054959467 ) ) ;
#13878=DIRECTION ( 'NONE',  ( -1.177540334020096294E-17, 0.2588190451025213501, -0.9659258262890680902 ) ) ;
#13905=ORIENTED_EDGE ( 'NONE', *, *, #13192, .T. ) ;
#13913=AXIS2_PLACEMENT_3D ( 'NONE', #3558, #9170, #16615 ) ;
#13987=CARTESIAN_POINT ( 'NONE',  ( -0.1114086484834320989, 0.7676189894794268609, -1.079857323803883107 ) ) ;
#14008=CARTESIAN_POINT ( 'NONE',  ( 0.000000000000000000, 0.9300000000000000488, 0.000000000000000000 ) ) ;
#14102=CARTESIAN_POINT ( 'NONE',  ( -0.1580085009183549993, 0.7453923191467759501, -1.080137057852694538 ) ) ;
#14109=CARTESIAN_POINT ( 'NONE',  ( 0.000000000000000000, 0.8949999999999999067, 1.015181661097394050 ) ) ;
#14191=AXIS2_PLACEMENT_3D ( 'NONE', #16869, #278, #157 ) ;
#14203=PRODUCT_DEFINITION_SHAPE ( 'NONE', 'NONE',  #2989 ) ;
#14220=CARTESIAN_POINT ( 'NONE',  ( -0.04142811702957077680, 0.7863941770016692479, -1.079911001309288299 ) ) ;
#14273=CARTESIAN_POINT ( 'NONE',  ( -0.1820207676368335581, 0.4792642385880945821, -0.7276181116126451132 ) ) ;
#14294=ORIENTED_EDGE ( 'NONE', *, *, #20324, .T. ) ;
#14336=ORIENTED_EDGE ( 'NONE', *, *, #13407, .T. ) ;
#14357=ADVANCED_FACE ( 'NONE', ( #19846, #10235 ), #10476, .T. ) ;
#14397=CARTESIAN_POINT ( 'NONE',  ( -0.1066700245536902208, 0.5609335224602052250, -0.7424636365021335394 ) ) ;
#14417=CIRCLE ( 'NONE', #3510, 0.03500000000000003803 ) ;
#14463=CARTESIAN_POINT ( 'NONE',  ( 0.1293617830085710407, 0.5441123095027139422, -0.7388485444064273322 ) ) ;
#14517=CARTESIAN_POINT ( 'NONE',  ( -0.1669947351848384554, 0.5031321662965324570, -0.7312129885460184608 ) ) ;
#14566=EDGE_CURVE ( 'NONE', #5262, #19113, #7883, .T. ) ;
#14579=DIRECTION ( 'NONE',  ( 0.000000000000000000, 1.000000000000000000, 0.000000000000000000 ) ) ;
#14582=CARTESIAN_POINT ( 'NONE',  ( 0.2019315168632336566, 0.3017797859643823188, -0.7223231963670132538 ) ) ;
#14642=CARTESIAN_POINT ( 'NONE',  ( -0.2055620820422562611, 0.3152427873485467158, -0.7212836743131715300 ) ) ;
#14655=EDGE_LOOP ( 'NONE', ( #3309, #10986, #11543, #23991 ) ) ;
#14659=DIRECTION ( 'NONE',  ( 0.000000000000000000, 0.000000000000000000, 1.000000000000000000 ) ) ;
#14696=EDGE_CURVE ( 'NONE', #18852, #11248, #15261, .T. ) ;
#14708=CARTESIAN_POINT ( 'NONE',  ( 0.000000000000000000, 0.9300000000000000488, 0.000000000000000000 ) ) ;
#14713=ORIENTED_EDGE ( 'NONE', *, *, #11728, .F. ) ;
#14756=VECTOR ( 'NONE', #20422, 39.37007874015748854 ) ;
#14767=CARTESIAN_POINT ( 'NONE',  ( -0.1585368710484967580, 0.5142162655923535608, -0.7331154209853633086 ) ) ;
#14829=ORIENTED_EDGE ( 'NONE', *, *, #11755, .F. ) ;
#14895=EDGE_CURVE ( 'NONE', #5067, #19113, #18725, .T. ) ;
#14939=CARTESIAN_POINT ( 'NONE',  ( 0.000000000000000000, 0.8949999999999999067, 0.000000000000000000 ) ) ;
#14942=EDGE_LOOP ( 'NONE', ( #4997, #7845, #15161, #11249 ) ) ;
#14996=CARTESIAN_POINT ( 'NONE',  ( -1.522235971340160240E-16, 0.1799999999999999933, -1.243000000000000105 ) ) ;
#15121=CARTESIAN_POINT ( 'NONE',  ( 0.000000000000000000, 0.01999999999999951469, 0.000000000000000000 ) ) ;
#15122=CARTESIAN_POINT ( 'NONE',  ( 0.3149902191487801151, 0.4934499048855510717, -1.115388133222527722 ) ) ;
#15152=CARTESIAN_POINT ( 'NONE',  ( -1.322549964794167179E-16, 0.7885332705621128646, -1.079944001585411595 ) ) ;
#15161=ORIENTED_EDGE ( 'NONE', *, *, #14895, .F. ) ;
#15237=CARTESIAN_POINT ( 'NONE',  ( 0.04147192196593674912, 0.7863862574794888705, -1.079910930672920655 ) ) ;
#15243=EDGE_CURVE ( 'NONE', #11248, #19113, #470, .T. ) ;
#15258=ORIENTED_EDGE ( 'NONE', *, *, #13809, .T. ) ;
#15261=B_SPLINE_CURVE_WITH_KNOTS ( 'NONE', 3,
 ( #21530, #15921, #14220, #4818, #3122, #4944, #13987, #23225, #14102, #6534, #8479, #23467, #21657, #12408, #811, #10573, #23344, #6655, #21414, #17758, #12171, #12288, #19827, #2646, #19579, #6415, #15692, #13869, #2872, #16052, #17881, #10095, #10331, #3005, #12049, #1173, #21296, #8611, #4590, #6777, #17516, #19462, #17637, #926 ),
 .UNSPECIFIED., .F., .F.,
 ( 4, 2, 2, 2, 2, 2, 2, 2, 2, 2, 2, 2, 2, 2, 2, 2, 2, 2, 2, 2, 2, 4 ),
 ( 0.03213067753877397320, 0.03370072127975529824, 0.03448574315024595383, 0.03527076502073661635, 0.03684080876171794139, 0.03762583063220859697, 0.03841085250269925255, 0.03998089624368057760, 0.04155093998466190264, 0.04233596185515256516, 0.04312098372564323462, 0.04469102746662455966, 0.04626107120760588470, 0.04783111494858721668, 0.04861613681907787921, 0.04940115868956854173, 0.05097120243054986677, 0.05254124617153120569, 0.05332626804202186821, 0.05411128991251254461, 0.05568133365349388353, 0.05725137739447521551 ),
 .UNSPECIFIED. ) ;
#15319=FACE_OUTER_BOUND ( 'NONE', #3518, .T. ) ;
#15335=CARTESIAN_POINT ( 'NONE',  ( 1.522235971340160240E-16, 0.01999999999999951469, -1.243000000000000105 ) ) ;
#15354=CARTESIAN_POINT ( 'NONE',  ( 0.1018054737164394014, 0.1946304594345829864, -1.235041780627553987 ) ) ;
#15474=CARTESIAN_POINT ( 'NONE',  ( 0.000000000000000000, 0.1799999999999999933, -1.243000000000000105 ) ) ;
#15523=( NAMED_UNIT ( * ) PLANE_ANGLE_UNIT ( ) SI_UNIT ( $, .RADIAN. ) );
#15568=DIRECTION ( 'NONE',  ( 0.000000000000000000, 1.000000000000000000, 0.000000000000000000 ) ) ;
#15599=PLANE ( 'NONE',  #8663 ) ;
#15657=DIRECTION ( 'NONE',  ( -0.000000000000000000, -1.000000000000000000, -0.000000000000000000 ) ) ;
#15692=CARTESIAN_POINT ( 'NONE',  ( -0.2989142788957511176, 0.3766842777223494143, -1.152193287665570942 ) ) ;
#15693=CARTESIAN_POINT ( 'NONE',  ( 9.184850993605150903E-17, 0.000000000000000000, -0.7500000000000001110 ) ) ;
#15703=AXIS2_PLACEMENT_3D ( 'NONE', #8343, #21286, #15909 ) ;
#15707=ADVANCED_FACE ( 'NONE', ( #19249, #22339 ), #15599, .T. ) ;
#15804=CARTESIAN_POINT ( 'NONE',  ( 0.000000000000000000, 0.1799999999999999933, 0.000000000000000000 ) ) ;
#15813=CARTESIAN_POINT ( 'NONE',  ( -1.399103805173478513E-17, 0.4635611116728546865, -1.084197934689580034 ) ) ;
#15816=CARTESIAN_POINT ( 'NONE',  ( 0.000000000000000000, 0.000000000000000000, 0.000000000000000000 ) ) ;
#15877=CARTESIAN_POINT ( 'NONE',  ( 0.000000000000000000, 0.1799999999999999933, 0.000000000000000000 ) ) ;
#15878=CARTESIAN_POINT ( 'NONE',  ( 0.000000000000000000, 0.000000000000000000, 0.000000000000000000 ) ) ;
#15901=ORIENTED_EDGE ( 'NONE', *, *, #11798, .T. ) ;
#15909=DIRECTION ( 'NONE',  ( 0.000000000000000000, 0.9659258262890680902, 0.2588190451025215721 ) ) ;
#15912=CARTESIAN_POINT ( 'NONE',  ( 9.184120737366631376E-17, 0.1556215347031258134, -0.7500000000000001110 ) ) ;
#15921=CARTESIAN_POINT ( 'NONE',  ( -0.02089153872600517728, 0.7885332705621130867, -1.079944001585411373 ) ) ;
#16038=DIRECTION ( 'NONE',  ( -1.177540334020096294E-17, 0.2588190451025213501, -0.9659258262890682012 ) ) ;
#16052=CARTESIAN_POINT ( 'NONE',  ( -0.2728196097062217662, 0.3240212061204770788, -1.173116651927777365 ) ) ;
#16102=CARTESIAN_POINT ( 'NONE',  ( -0.2105386197592548914, 0.3855283470628421694, -0.7198427731174872335 ) ) ;
#16153=EDGE_CURVE ( 'NONE', #10527, #3971, #5147, .T. ) ;
#16163=CARTESIAN_POINT ( 'NONE',  ( 0.01427445631846820454, 0.5924045552181391727, -0.7500000000000002220 ) ) ;
#16227=CARTESIAN_POINT ( 'NONE',  ( -0.1290899616220235746, 0.5438854779856191479, -0.7388258714505984148 ) ) ;
#16339=CARTESIAN_POINT ( 'NONE',  ( 2.114905110478964667E-17, 0.5924045552181390617, -0.7500000000000001110 ) ) ;
#16373=VERTEX_POINT ( 'NONE', #15693 ) ;
#16411=CARTESIAN_POINT ( 'NONE',  ( 0.1884737858362492136, 0.4666198245431632530, -0.7259526178673825214 ) ) ;
#16458=DIRECTION ( 'NONE',  ( 0.000000000000000000, 0.000000000000000000, 1.000000000000000000 ) ) ;
#16464=CARTESIAN_POINT ( 'NONE',  ( 2.114905110478964667E-17, 0.5924045552181390617, -0.7500000000000001110 ) ) ;
#16585=CARTESIAN_POINT ( 'NONE',  ( -0.05588159907449195135, 0.5841765427403826649, -0.7479453483804153757 ) ) ;
#16615=DIRECTION ( 'NONE',  ( 0.000000000000000000, 0.000000000000000000, 1.000000000000000000 ) ) ;
#16748=CARTESIAN_POINT ( 'NONE',  ( 0.000000000000000000, 0.000000000000000000, 0.000000000000000000 ) ) ;
#16781=EDGE_CURVE ( 'NONE', #16373, #7491, #1293, .T. ) ;
#16821=DIRECTION ( 'NONE',  ( 0.000000000000000000, 1.000000000000000000, 0.000000000000000000 ) ) ;
#16869=CARTESIAN_POINT ( 'NONE',  ( 0.000000000000000000, 0.1799999999999999933, 0.000000000000000000 ) ) ;
#16926=ORIENTED_EDGE ( 'NONE', *, *, #16153, .F. ) ;
#17003=AXIS2_PLACEMENT_3D ( 'NONE', #11452, #5948, #2303 ) ;
#17051=CIRCLE ( 'NONE', #8078, 0.03500000000000003803 ) ;
#17087=MANIFOLD_SOLID_BREP ( '1/2-13 Tapped Hole', #1412 ) ;
#17131=CIRCLE ( 'NONE', #7398, 1.048989065017511546 ) ;
#17185=CARTESIAN_POINT ( 'NONE',  ( 0.2375040497016436547, 0.2775713580457571661, -1.193554297574972001 ) ) ;
#17244=CARTESIAN_POINT ( 'NONE',  ( 9.184850993605150903E-17, -3.937007874019685528E-05, -0.7500000000000001110 ) ) ;
#17263=ORIENTED_EDGE ( 'NONE', *, *, #4056, .T. ) ;
#17265=ORIENTED_EDGE ( 'NONE', *, *, #12577, .F. ) ;
#17268=CARTESIAN_POINT ( 'NONE',  ( 0.000000000000000000, 0.01999999999999951469, 0.000000000000000000 ) ) ;
#17299=CARTESIAN_POINT ( 'NONE',  ( 0.2870356121319265763, 0.3498146942408093540, -1.162598210319561343 ) ) ;
#17373=AXIS2_PLACEMENT_3D ( 'NONE', #6217, #21570, #12329 ) ;
#17409=DIRECTION ( 'NONE',  ( 0.000000000000000000, 0.000000000000000000, 1.000000000000000000 ) ) ;
#17487=AXIS2_PLACEMENT_3D ( 'NONE', #23222, #15568, #10208 ) ;
#17516=CARTESIAN_POINT ( 'NONE',  ( -0.08208998203245540526, 0.1891853512034874507, -1.237990233360560355 ) ) ;
#17560=CIRCLE ( 'NONE', #7046, 0.2109499999999996100 ) ;
#17586=DIRECTION ( 'NONE',  ( -0.000000000000000000, -1.000000000000000000, -0.000000000000000000 ) ) ;
#17616=ORIENTED_EDGE ( 'NONE', *, *, #9970, .F. ) ;
#17632=DIRECTION ( 'NONE',  ( 0.000000000000000000, 0.000000000000000000, -1.000000000000000000 ) ) ;
#17637=CARTESIAN_POINT ( 'NONE',  ( -0.02060854148827287805, 0.1800000000000000211, -1.243000000000000327 ) ) ;
#17652=CARTESIAN_POINT ( 'NONE',  ( 0.000000000000000000, 0.9300000000000000488, 0.7700000000000013500 ) ) ;
#17748=CARTESIAN_POINT ( 'NONE',  ( 0.2112257014698199487, 0.3573301435892229927, -0.7196414598378356731 ) ) ;
#17758=CARTESIAN_POINT ( 'NONE',  ( -0.3043026786824803431, 0.5532075493895395324, -1.101750068115465941 ) ) ;
#17867=CYLINDRICAL_SURFACE ( 'NONE', #9131, 0.3150000000000000577 ) ;
#17873=CARTESIAN_POINT ( 'NONE',  ( 0.06947902941946425270, 0.1664576461568605392, -0.7468889270519576407 ) ) ;
#17881=CARTESIAN_POINT ( 'NONE',  ( -0.2675307584405086092, 0.3158328359438148381, -1.176588187136770491 ) ) ;
#17901=ADVANCED_FACE ( 'NONE', ( #4733 ), #2085, .F. ) ;
#17933=CARTESIAN_POINT ( 'NONE',  ( -0.04900341404797774192, 0.5861343809992684006, -0.7484292681947780634 ) ) ;
#17962=EDGE_CURVE ( 'NONE', #23184, #6211, #12226, .T. ) ;
#17995=CARTESIAN_POINT ( 'NONE',  ( 0.09469217842228347393, 0.5681098745337339606, -0.7441083818505032088 ) ) ;
#18069=ORIENTED_EDGE ( 'NONE', *, *, #1578, .T. ) ;
#18112=CARTESIAN_POINT ( 'NONE',  ( 0.1586331323214220657, 0.5141020712338113530, -0.7330949616466568841 ) ) ;
#18170=CARTESIAN_POINT ( 'NONE',  ( -0.05603163257930598301, 0.1624274118792091159, -0.7480337429100453184 ) ) ;
#18283=CARTESIAN_POINT ( 'NONE',  ( 0.000000000000000000, -3.937007874019685528E-05, 0.000000000000000000 ) ) ;
#18290=CARTESIAN_POINT ( 'NONE',  ( -0.1884161264613055942, 0.4667385597628443406, -0.7259675891464789643 ) ) ;
#18409=CARTESIAN_POINT ( 'NONE',  ( -0.06925083771014352296, 0.5795781470845841055, -0.7468261636789826907 ) ) ;
#18468=CARTESIAN_POINT ( 'NONE',  ( 0.000000000000000000, 0.9099999999999988098, 0.000000000000000000 ) ) ;
#18487=CIRCLE ( 'NONE', #8741, 1.223000000000000309 ) ;
#18495=EDGE_LOOP ( 'NONE', ( #23848, #9948, #12297, #11627, #2115 ) ) ;
#18574=CIRCLE ( 'NONE', #13913, 1.243000000000000105 ) ;
#18647=CARTESIAN_POINT ( 'NONE',  ( 0.2727677001506427223, 0.6283691918605152082, -1.089234312191128540 ) ) ;
#18690=VECTOR ( 'NONE', #9419, 39.37007874015747433 ) ;
#18725=CIRCLE ( 'NONE', #21834, 1.243000000000000105 ) ;
#18727=CARTESIAN_POINT ( 'NONE',  ( 9.184850993605150903E-17, 0.9099999999999988098, -0.7500000000000001110 ) ) ;
#18757=ORIENTED_EDGE ( 'NONE', *, *, #2836, .T. ) ;
#18768=CARTESIAN_POINT ( 'NONE',  ( 0.2082036761074528841, 0.7085065112206522242, -1.081619176768333412 ) ) ;
#18825=ORIENTED_EDGE ( 'NONE', *, *, #11935, .T. ) ;
#18852=VERTEX_POINT ( 'NONE', #15152 ) ;
#18855=CIRCLE ( 'NONE', #932, 0.7700000000000013500 ) ;
#18877=CONICAL_SURFACE ( 'NONE', #7949, 1.243000000000000105, 0.2617993877991500740 ) ;
#18894=CARTESIAN_POINT ( 'NONE',  ( 0.3129372601465110204, 0.4335988933679512103, -1.132625307779410395 ) ) ;
#18909=AXIS2_PLACEMENT_3D ( 'NONE', #12395, #3223, #19812 ) ;
#18966=CARTESIAN_POINT ( 'NONE',  ( 1.243238971816016674E-16, 0.8949999999999999067, -1.015181661097394050 ) ) ;
#18978=CARTESIAN_POINT ( 'NONE',  ( 1.509989503348686489E-16, 0.000000000000000000, -1.223000000000000309 ) ) ;
#19015=CARTESIAN_POINT ( 'NONE',  ( 0.3150097106828184113, 0.4536608415932815164, -1.126457079336245393 ) ) ;
#19090=DIRECTION ( 'NONE',  ( -0.000000000000000000, 1.000000000000000000, -0.000000000000000000 ) ) ;
#19113=VERTEX_POINT ( 'NONE', #23047 ) ;
#19120=CIRCLE ( 'NONE', #3156, 1.048989065017511546 ) ;
#19126=CARTESIAN_POINT ( 'NONE',  ( 0.1015149863201169345, 0.7712941925382441610, -1.079846890036118667 ) ) ;
#19249=FACE_BOUND ( 'NONE', #10924, .T. ) ;
#19411=CARTESIAN_POINT ( 'NONE',  ( 0.000000000000000000, 0.9040586665785882436, 0.000000000000000000 ) ) ;
#19462=CARTESIAN_POINT ( 'NONE',  ( -0.04114923329550543296, 0.1818063343982506408, -1.242004357290043881 ) ) ;
#19475=CARTESIAN_POINT ( 'NONE',  ( 0.000000000000000000, 0.9300000000000000488, 1.015181661097394050 ) ) ;
#19510=DIRECTION ( 'NONE',  ( 0.000000000000000000, 0.9659258262890680902, 0.2588190451025215721 ) ) ;
#19579=CARTESIAN_POINT ( 'NONE',  ( -0.3129466533217430957, 0.4336677069265437723, -1.132603556623053231 ) ) ;
#19717=EDGE_CURVE ( 'NONE', #22559, #10294, #18855, .T. ) ;
#19759=CARTESIAN_POINT ( 'NONE',  ( -0.02831565414742191061, 0.5908090236396409400, -0.7495925827047090761 ) ) ;
#19812=DIRECTION ( 'NONE',  ( 0.000000000000000000, 0.000000000000000000, -1.000000000000000000 ) ) ;
#19813=DIRECTION ( 'NONE',  ( 0.000000000000000000, 1.000000000000000000, 0.000000000000000000 ) ) ;
#19818=CARTESIAN_POINT ( 'NONE',  ( 2.114905110478964667E-17, 0.5924045552181390617, -0.7500000000000001110 ) ) ;
#19827=CARTESIAN_POINT ( 'NONE',  ( -0.3149849110527242479, 0.4935441587820288967, -1.115363383729591540 ) ) ;
#19846=FACE_BOUND ( 'NONE', #5417, .T. ) ;
#19865=ADVANCED_BREP_SHAPE_REPRESENTATION ( '', ( #17087, #9127 ), #2886 ) ;
#19867=B_SPLINE_CURVE_WITH_KNOTS ( 'NONE', 3,
 ( #11586, #236, #20837, #7902, #20717, #2311, #15354, #13543, #6077, #11339, #7672, #5839, #9872, #17185, #21076, #6195, #4013, #4366, #17299, #11703, #9626, #18894, #19015, #15122, #109, #13302, #22548, #2195, #11461, #352, #13185, #18647, #5726, #20958, #2063, #18768, #4251, #1940, #9748, #9387, #19126, #7793, #2430, #15237, #592, #22666 ),
 .UNSPECIFIED., .F., .F.,
 ( 4, 2, 2, 2, 2, 2, 2, 2, 2, 2, 2, 2, 2, 2, 2, 2, 2, 2, 2, 2, 2, 2, 4 ),
 ( 0.007005524140355982865, 0.007790685184056548099, 0.008575846227757113333, 0.01014616831515824553, 0.01093132935885880903, 0.01171649040255937427, 0.01328681248996050820, 0.01485713457736164041, 0.01564229562106220217, 0.01642745666476276914, 0.01799777875216388573, 0.01956810083956500579, 0.02113842292696612585, 0.02192358397066668935, 0.02270874501436724591, 0.02349390605806780941, 0.02427906710176836944, 0.02584938918916948949, 0.02741971127657060955, 0.02899003336397173308, 0.02977519440767229658, 0.03056035545137285314, 0.03213067753877397320 ),
 .UNSPECIFIED. ) ;
#19942=CARTESIAN_POINT ( 'NONE',  ( 0.2102303072135171258, 0.3429911158895919132, -0.7199368671688829435 ) ) ;
#19999=CARTESIAN_POINT ( 'NONE',  ( -0.1701069292077561357, 0.2394183616649627200, -0.7304681109799713301 ) ) ;
#20011=CARTESIAN_POINT ( 'NONE',  ( 1.522235971340160240E-16, 0.1799999999999999933, 1.243000000000000105 ) ) ;
#20062=CARTESIAN_POINT ( 'NONE',  ( 0.05604628919722569325, 0.1624317956547894071, -0.7480325013175007642 ) ) ;
#20064=ORIENTED_EDGE ( 'NONE', *, *, #2471, .F. ) ;
#20120=CARTESIAN_POINT ( 'NONE',  ( -0.2102330194709680078, 0.3429979575999043684, -0.7199360985034549687 ) ) ;
#20163=EDGE_CURVE ( 'NONE', #11248, #4141, #22360, .T. ) ;
#20192=DIRECTION ( 'NONE',  ( 0.000000000000000000, 0.000000000000000000, 1.000000000000000000 ) ) ;
#20324=EDGE_CURVE ( 'NONE', #428, #4141, #20882, .T. ) ;
#20344=ORIENTED_EDGE ( 'NONE', *, *, #11935, .F. ) ;
#20354=DIRECTION ( 'NONE',  ( 0.000000000000000000, 0.000000000000000000, 1.000000000000000000 ) ) ;
#20363=ORIENTED_EDGE ( 'NONE', *, *, #19717, .F. ) ;
#20374=ORIENTED_EDGE ( 'NONE', *, *, #975, .F. ) ;
#20422=DIRECTION ( 'NONE',  ( 0.000000000000000000, 0.7071067811865474617, 0.7071067811865474617 ) ) ;
#20530=ADVANCED_FACE ( 'NONE', ( #2482 ), #18877, .T. ) ;
#20537=LINE ( 'NONE', #3833, #11634 ) ;
#20594=ADVANCED_FACE ( 'NONE', ( #6973 ), #3278, .T. ) ;
#20639=AXIS2_PLACEMENT_3D ( 'NONE', #15813, #13878, #23473 ) ;
#20648=AXIS2_PLACEMENT_3D ( 'NONE', #10088, #2754, #10569 ) ;
#20652=ORIENTED_EDGE ( 'NONE', *, *, #23118, .T. ) ;
#20708=CYLINDRICAL_SURFACE ( 'NONE', #17003, 0.7500000000000001110 ) ;
#20717=CARTESIAN_POINT ( 'NONE',  ( 0.05168019678275902890, 0.1836979246868377935, -1.240975288036999080 ) ) ;
#20837=CARTESIAN_POINT ( 'NONE',  ( 0.02062928380395624012, 0.1804553015353551615, -1.242749888402949976 ) ) ;
#20882=LINE ( 'NONE', #22832, #2125 ) ;
#20887=B_SPLINE_CURVE_WITH_KNOTS ( 'NONE', 3,
 ( #19818, #16163, #23697, #5054, #8604, #17995, #10806, #14463, #21885, #18112, #1531, #12523, #16411, #23579, #3115, #21647, #23819, #17748, #19942, #7141, #14582, #1287, #1043, #22004, #21520, #4936, #5304, #5176, #6646, #3229, #12645, #17873, #20062, #12767, #2862, #10324, #8472, #15912 ),
 .UNSPECIFIED., .F., .F.,
 ( 4, 2, 2, 2, 2, 2, 2, 2, 2, 2, 2, 2, 2, 2, 2, 2, 2, 2, 4 ),
 ( 1.321750921635994236E-18, 0.001070994599891817887, 0.002141989199783634473, 0.003212983799675450409, 0.004283978399567268079, 0.005354972999459083581, 0.006425967599350898216, 0.007496962199242714585, 0.008567956799134529219, 0.009638951399026346456, 0.01070994599891816369, 0.01124544329886406971, 0.01178094059880997573, 0.01285193519870178776, 0.01392292979859359979, 0.01499392439848541356, 0.01606491899837722559, 0.01660041629832313334, 0.01713591359826903762 ),
 .UNSPECIFIED. ) ;
#20953=EDGE_CURVE ( 'NONE', #5711, #5262, #18487, .T. ) ;
#20958=CARTESIAN_POINT ( 'NONE',  ( 0.2501637473317315230, 0.6631371529007064058, -1.085132529289236425 ) ) ;
#21033=ORIENTED_EDGE ( 'NONE', *, *, #11314, .T. ) ;
#21058=DIRECTION ( 'NONE',  ( 0.000000000000000000, 1.000000000000000000, 0.000000000000000000 ) ) ;
#21076=CARTESIAN_POINT ( 'NONE',  ( 0.2505061212867025211, 0.2922223361170756539, -1.186846436122991788 ) ) ;
#21133=EDGE_LOOP ( 'NONE', ( #3244, #21182, #14294, #15901, #12128 ) ) ;
#21182=ORIENTED_EDGE ( 'NONE', *, *, #8297, .T. ) ;
#21220=CARTESIAN_POINT ( 'NONE',  ( 0.000000000000000000, 0.9040586665785882436, 1.048989065017511546 ) ) ;
#21255=CIRCLE ( 'NONE', #11130, 1.015181661097394050 ) ;
#21261=LINE ( 'NONE', #17244, #775 ) ;
#21286=DIRECTION ( 'NONE',  ( -1.177540334020096294E-17, 0.2588190451025213501, -0.9659258262890680902 ) ) ;
#21296=CARTESIAN_POINT ( 'NONE',  ( -0.1577217838551094042, 0.2181752645060030527, -1.222675257892397838 ) ) ;
#21330=DIRECTION ( 'NONE',  ( -0.000000000000000000, -1.000000000000000000, -0.000000000000000000 ) ) ;
#21377=ORIENTED_EDGE ( 'NONE', *, *, #13407, .F. ) ;
#21394=EDGE_LOOP ( 'NONE', ( #5538, #14829, #6484, #22970 ) ) ;
#21403=AXIS2_PLACEMENT_3D ( 'NONE', #16748, #29, #7476 ) ;
#21407=ADVANCED_FACE ( 'NONE', ( #15319 ), #9543, .T. ) ;
#21414=CARTESIAN_POINT ( 'NONE',  ( -0.2982593250668997276, 0.5727001298589282641, -1.097990058363176535 ) ) ;
#21440=CARTESIAN_POINT ( 'NONE',  ( -1.399103805173478513E-17, 0.4635611116728546865, -1.084197934689580034 ) ) ;
#21508=EDGE_LOOP ( 'NONE', ( #7484, #11618, #20363, #22544 ) ) ;
#21520=CARTESIAN_POINT ( 'NONE',  ( 0.1817294119778012085, 0.2568935841375707407, -0.7276602140724116596 ) ) ;
#21530=CARTESIAN_POINT ( 'NONE',  ( -1.322549964794167179E-16, 0.7885332705621128646, -1.079944001585411595 ) ) ;
#21570=DIRECTION ( 'NONE',  ( -0.000000000000000000, 1.000000000000000000, -0.000000000000000000 ) ) ;
#21647=CARTESIAN_POINT ( 'NONE',  ( 0.2089035349127157382, 0.3994243068236463801, -0.7203251050642737185 ) ) ;
#21657=CARTESIAN_POINT ( 'NONE',  ( -0.2154970682147052952, 0.7011027796760176400, -1.082144637830705358 ) ) ;
#21664=ORIENTED_EDGE ( 'NONE', *, *, #15243, .T. ) ;
#21667=ADVANCED_FACE ( 'NONE', ( #12272 ), #17867, .F. ) ;
#21677=DIRECTION ( 'NONE',  ( 0.000000000000000000, 0.7071067811865426878, 0.7071067811865523467 ) ) ;
#21833=ADVANCED_FACE ( 'NONE', ( #1757 ), #5169, .T. ) ;
#21834=AXIS2_PLACEMENT_3D ( 'NONE', #15121, #7435, #5229 ) ;
#21885=CARTESIAN_POINT ( 'NONE',  ( 0.1397624911352057520, 0.5346735903725252648, -0.7369254640284191860 ) ) ;
#21957=CARTESIAN_POINT ( 'NONE',  ( 0.000000000000000000, 0.1799999999999999933, 0.000000000000000000 ) ) ;
#22004=CARTESIAN_POINT ( 'NONE',  ( 0.1851914621056884036, 0.2629614562125153210, -0.7267838718924568564 ) ) ;
#22056=FACE_OUTER_BOUND ( 'NONE', #22632, .T. ) ;
#22173=EDGE_CURVE ( 'NONE', #412, #18852, #1580, .T. ) ;
#22176=DIRECTION ( 'NONE',  ( -3.169619151431772953E-17, -0.9659258262890682012, -0.2588190451025213501 ) ) ;
#22177=CYLINDRICAL_SURFACE ( 'NONE', #5045, 0.7500000000000001110 ) ;
#22183=CARTESIAN_POINT ( 'NONE',  ( -0.1079887943494003133, 0.1837715311241617522, -0.7422780453074593332 ) ) ;
#22226=CARTESIAN_POINT ( 'NONE',  ( 0.000000000000000000, 0.1799999999999999933, 0.000000000000000000 ) ) ;
#22241=DIRECTION ( 'NONE',  ( 0.000000000000000000, 1.000000000000000000, 0.000000000000000000 ) ) ;
#22339=FACE_OUTER_BOUND ( 'NONE', #222, .T. ) ;
#22360=CIRCLE ( 'NONE', #14191, 1.243000000000000105 ) ;
#22418=DIRECTION ( 'NONE',  ( 0.000000000000000000, 0.9659258262890680902, 0.2588190451025214611 ) ) ;
#22487=CARTESIAN_POINT ( 'NONE',  ( 9.184850993605150903E-17, -3.937007874019685528E-05, -0.7500000000000001110 ) ) ;
#22524=DIRECTION ( 'NONE',  ( -1.177540334020096294E-17, 0.2588190451025213501, -0.9659258262890680902 ) ) ;
#22544=ORIENTED_EDGE ( 'NONE', *, *, #6620, .F. ) ;
#22548=CARTESIAN_POINT ( 'NONE',  ( 0.3043093620448166226, 0.5531817298998159549, -1.101755390420818603 ) ) ;
#22559=VERTEX_POINT ( 'NONE', #17652 ) ;
#22601=SHAPE_DEFINITION_REPRESENTATION ( #14203, #1861 ) ;
#22632=EDGE_LOOP ( 'NONE', ( #18825, #14336, #4321, #9803, #13905, #14713 ) ) ;
#22659=FACE_OUTER_BOUND ( 'NONE', #4395, .T. ) ;
#22666=CARTESIAN_POINT ( 'NONE',  ( -1.322549964794167179E-16, 0.7885332705621128646, -1.079944001585411595 ) ) ;
#22832=CARTESIAN_POINT ( 'NONE',  ( 0.000000000000000000, 0.1799999999999999933, 1.243000000000000105 ) ) ;
#22840=EDGE_LOOP ( 'NONE', ( #5122, #12674, #21664, #18069 ) ) ;
#22881=FACE_OUTER_BOUND ( 'NONE', #21394, .T. ) ;
#22892=UNCERTAINTY_MEASURE_WITH_UNIT (LENGTH_MEASURE( 1.000000000000000082E-05 ), #6246, 'distance_accuracy_value', 'NONE');
#22929=CONICAL_SURFACE ( 'NONE', #17487, 0.7500000000000001110, 0.7853981633974482790 ) ;
#22970=ORIENTED_EDGE ( 'NONE', *, *, #23118, .F. ) ;
#23022=CARTESIAN_POINT ( 'NONE',  ( 0.000000000000000000, 0.9300000000000000488, 0.000000000000000000 ) ) ;
#23029=EDGE_LOOP ( 'NONE', ( #20374, #24070, #23085, #3230 ) ) ;
#23047=CARTESIAN_POINT ( 'NONE',  ( 0.000000000000000000, 0.01999999999999951469, -1.243000000000000105 ) ) ;
#23085=ORIENTED_EDGE ( 'NONE', *, *, #6620, .T. ) ;
#23095=CYLINDRICAL_SURFACE ( 'NONE', #394, 0.2109499999999996656 ) ;
#23113=CARTESIAN_POINT ( 'NONE',  ( 9.184850993605150903E-17, 0.9099999999999988098, -0.7500000000000001110 ) ) ;
#23118=EDGE_CURVE ( 'NONE', #12482, #795, #21255, .T. ) ;
#23125=CARTESIAN_POINT ( 'NONE',  ( 9.184120737366631376E-17, 0.1556215347031258134, -0.7500000000000001110 ) ) ;
#23146=AXIS2_PLACEMENT_3D ( 'NONE', #17268, #19090, #72 ) ;
#23181=DIRECTION ( 'NONE',  ( 0.000000000000000000, 0.000000000000000000, 1.000000000000000000 ) ) ;
#23184=VERTEX_POINT ( 'NONE', #10265 ) ;
#23222=CARTESIAN_POINT ( 'NONE',  ( 0.000000000000000000, 0.9099999999999988098, 0.000000000000000000 ) ) ;
#23225=CARTESIAN_POINT ( 'NONE',  ( -0.1399538861531764988, 0.7553620363409487837, -1.079965667524036776 ) ) ;
#23293=DIRECTION ( 'NONE',  ( -0.000000000000000000, -1.000000000000000000, -0.000000000000000000 ) ) ;
#23294=DIRECTION ( 'NONE',  ( 1.000000000000000000, 0.000000000000000000, 0.000000000000000000 ) ) ;
#23344=CARTESIAN_POINT ( 'NONE',  ( -0.2829524303836037369, 0.6104264140268672589, -1.091612836571470568 ) ) ;
#23346=DIRECTION ( 'NONE',  ( 0.000000000000000000, 0.9659258262890680902, 0.2588190451025214611 ) ) ;
#23453=FACE_BOUND ( 'NONE', #13715, .T. ) ;
#23467=CARTESIAN_POINT ( 'NONE',  ( -0.2079132705422924166, 0.7081134582484001072, -1.081719846782932759 ) ) ;
#23473=DIRECTION ( 'NONE',  ( 0.000000000000000000, 0.9659258262890680902, 0.2588190451025215166 ) ) ;
#23516=CARTESIAN_POINT ( 'NONE',  ( -0.2019078322727933528, 0.3016929934852337625, -0.7223299880601123935 ) ) ;
#23579=CARTESIAN_POINT ( 'NONE',  ( 0.1989806073349426052, 0.4406257711794490106, -0.7231433393460605652 ) ) ;
#23639=CARTESIAN_POINT ( 'NONE',  ( -0.1312060371020148941, 0.1993095342438279682, -0.7385277598563807500 ) ) ;
#23657=LINE ( 'NONE', #5253, #1786 ) ;
#23697=CARTESIAN_POINT ( 'NONE',  ( 0.02825726476318201827, 0.5908114551644965129, -0.7495932795766503398 ) ) ;
#23814=EDGE_LOOP ( 'NONE', ( #11820, #5048 ) ) ;
#23819=CARTESIAN_POINT ( 'NONE',  ( 0.2105398893019958806, 0.3855051204502836781, -0.7198424012877072675 ) ) ;
#23848=ORIENTED_EDGE ( 'NONE', *, *, #11755, .T. ) ;
#23991=ORIENTED_EDGE ( 'NONE', *, *, #17962, .T. ) ;
#24070=ORIENTED_EDGE ( 'NONE', *, *, #12849, .F. ) ;
#24138=COLOUR_RGB('Deep Blue', 0.66274510, 0.83137255, 0.94901961);
#24139=FILL_AREA_STYLE_COLOUR('',#24138);
#24140=FILL_AREA_STYLE('',(#24139));
#24141=SURFACE_STYLE_FILL_AREA(#24140);
#24142=SURFACE_SIDE_STYLE('',(#24141));
#24143=SURFACE_STYLE_USAGE(.BOTH.,#24142);
#24144=PRESENTATION_STYLE_ASSIGNMENT((#24143));
#24192=STYLED_ITEM('',(#24144),#17087);
#24193=MECHANICAL_DESIGN_GEOMETRIC_PRESENTATION_REPRESENTATION('',(#24192),#2886);
ENDSEC;
END-ISO-10303-21;
